ISO-10303-21;
HEADER;
/* Generated by software containing ST-Developer
 * from STEP Tools, Inc. (www.steptools.com) 
 */

FILE_DESCRIPTION(
/* description */ ('STEP AP214'),
/* implementation_level */ '2;1');

FILE_NAME(
/* name */ 'Coupling Set Screw 1.step',
/* time_stamp */ '2026-11-15T14:55:55-08:00',
/* author */ (''),
/* organization */ (''),
/* preprocessor_version */ 'ST-DEVELOPER v20.2',
/* originating_system */ 'Autodesk Translation Framework v15.17.0.0',
/* authorisation */ '');

FILE_SCHEMA (('AUTOMOTIVE_DESIGN { 1 0 10303 214 3 1 1 }'));
ENDSEC;

DATA;
#10=MECHANICAL_DESIGN_GEOMETRIC_PRESENTATION_REPRESENTATION('',(#940),#57079);
#880=SHAPE_REPRESENTATION_RELATIONSHIP('SRR','None',#57268,#909);
#909=ADVANCED_BREP_SHAPE_REPRESENTATION('',(#977),#57060);
#940=STYLED_ITEM('',(#57444),#977);
#977=MANIFOLD_SOLID_BREP('Body1',#24540);
#1138=FACE_BOUND('',#4136,.T.);
#1541=PLANE('',#25645);
#1542=PLANE('',#25647);
#1543=PLANE('',#25650);
#1544=PLANE('',#25651);
#1545=PLANE('',#25652);
#1546=PLANE('',#25653);
#1547=PLANE('',#25654);
#1548=PLANE('',#25655);
#1549=PLANE('',#25656);
#2622=FACE_OUTER_BOUND('',#4135,.T.);
#2623=FACE_OUTER_BOUND('',#4137,.T.);
#2624=FACE_OUTER_BOUND('',#4138,.T.);
#2625=FACE_OUTER_BOUND('',#4139,.T.);
#2626=FACE_OUTER_BOUND('',#4140,.T.);
#2627=FACE_OUTER_BOUND('',#4141,.T.);
#2628=FACE_OUTER_BOUND('',#4142,.T.);
#2629=FACE_OUTER_BOUND('',#4143,.T.);
#2630=FACE_OUTER_BOUND('',#4144,.T.);
#2631=FACE_OUTER_BOUND('',#4145,.T.);
#4135=EDGE_LOOP('',(#18002));
#4136=EDGE_LOOP('',(#18003,#18004,#18005,#18006,#18007,#18008));
#4137=EDGE_LOOP('',(#18009));
#4138=EDGE_LOOP('',(#18010,#18011,#18012,#18013));
#4139=EDGE_LOOP('',(#18014,#18015,#18016,#18017,#18018,#18019));
#4140=EDGE_LOOP('',(#18020,#18021,#18022,#18023));
#4141=EDGE_LOOP('',(#18024,#18025,#18026,#18027));
#4142=EDGE_LOOP('',(#18028,#18029,#18030,#18031));
#4143=EDGE_LOOP('',(#18032,#18033,#18034,#18035));
#4144=EDGE_LOOP('',(#18036,#18037,#18038,#18039));
#4145=EDGE_LOOP('',(#18040,#18041,#18042,#18043));
#5720=LINE('',#51665,#7687);
#5721=LINE('',#51667,#7688);
#5722=LINE('',#51669,#7689);
#5723=LINE('',#51671,#7690);
#5724=LINE('',#51673,#7691);
#5725=LINE('',#51674,#7692);
#5726=LINE('',#51679,#7693);
#5727=LINE('',#51683,#7694);
#5728=LINE('',#51685,#7695);
#5729=LINE('',#51687,#7696);
#5730=LINE('',#51689,#7697);
#5731=LINE('',#51691,#7698);
#5732=LINE('',#51692,#7699);
#5733=LINE('',#51694,#7700);
#5734=LINE('',#51695,#7701);
#5735=LINE('',#51697,#7702);
#5736=LINE('',#51699,#7703);
#5737=LINE('',#51701,#7704);
#5738=LINE('',#51703,#7705);
#7687=VECTOR('',#29474,1000.);
#7688=VECTOR('',#29475,1000.);
#7689=VECTOR('',#29476,1000.);
#7690=VECTOR('',#29477,1000.);
#7691=VECTOR('',#29478,1000.);
#7692=VECTOR('',#29479,1000.);
#7693=VECTOR('',#29486,2.5);
#7694=VECTOR('',#29489,1000.);
#7695=VECTOR('',#29490,1000.);
#7696=VECTOR('',#29491,1000.);
#7697=VECTOR('',#29492,1000.);
#7698=VECTOR('',#29493,1000.);
#7699=VECTOR('',#29494,1000.);
#7700=VECTOR('',#29497,1000.);
#7701=VECTOR('',#29498,1000.);
#7702=VECTOR('',#29501,1000.);
#7703=VECTOR('',#29504,1000.);
#7704=VECTOR('',#29507,1000.);
#7705=VECTOR('',#29510,1000.);
#9552=CIRCLE('',#25646,2.5);
#9553=CIRCLE('',#25648,2.5);
#10933=VERTEX_POINT('',#51661);
#10934=VERTEX_POINT('',#51663);
#10935=VERTEX_POINT('',#51664);
#10936=VERTEX_POINT('',#51666);
#10937=VERTEX_POINT('',#51668);
#10938=VERTEX_POINT('',#51670);
#10939=VERTEX_POINT('',#51672);
#10940=VERTEX_POINT('',#51676);
#10941=VERTEX_POINT('',#51681);
#10942=VERTEX_POINT('',#51682);
#10943=VERTEX_POINT('',#51684);
#10944=VERTEX_POINT('',#51686);
#10945=VERTEX_POINT('',#51688);
#10946=VERTEX_POINT('',#51690);
#13546=EDGE_CURVE('',#10933,#10933,#9552,.T.);
#13547=EDGE_CURVE('',#10934,#10935,#5720,.T.);
#13548=EDGE_CURVE('',#10935,#10936,#5721,.T.);
#13549=EDGE_CURVE('',#10936,#10937,#5722,.T.);
#13550=EDGE_CURVE('',#10937,#10938,#5723,.T.);
#13551=EDGE_CURVE('',#10938,#10939,#5724,.T.);
#13552=EDGE_CURVE('',#10939,#10934,#5725,.T.);
#13553=EDGE_CURVE('',#10940,#10940,#9553,.T.);
#13554=EDGE_CURVE('',#10933,#10940,#5726,.T.);
#13555=EDGE_CURVE('',#10941,#10942,#5727,.T.);
#13556=EDGE_CURVE('',#10943,#10941,#5728,.T.);
#13557=EDGE_CURVE('',#10944,#10943,#5729,.T.);
#13558=EDGE_CURVE('',#10945,#10944,#5730,.T.);
#13559=EDGE_CURVE('',#10946,#10945,#5731,.T.);
#13560=EDGE_CURVE('',#10942,#10946,#5732,.T.);
#13561=EDGE_CURVE('',#10941,#10939,#5733,.T.);
#13562=EDGE_CURVE('',#10942,#10934,#5734,.T.);
#13563=EDGE_CURVE('',#10943,#10938,#5735,.T.);
#13564=EDGE_CURVE('',#10944,#10937,#5736,.T.);
#13565=EDGE_CURVE('',#10945,#10936,#5737,.T.);
#13566=EDGE_CURVE('',#10946,#10935,#5738,.T.);
#18002=ORIENTED_EDGE('',*,*,#13546,.T.);
#18003=ORIENTED_EDGE('',*,*,#13547,.T.);
#18004=ORIENTED_EDGE('',*,*,#13548,.T.);
#18005=ORIENTED_EDGE('',*,*,#13549,.T.);
#18006=ORIENTED_EDGE('',*,*,#13550,.T.);
#18007=ORIENTED_EDGE('',*,*,#13551,.T.);
#18008=ORIENTED_EDGE('',*,*,#13552,.T.);
#18009=ORIENTED_EDGE('',*,*,#13553,.T.);
#18010=ORIENTED_EDGE('',*,*,#13546,.F.);
#18011=ORIENTED_EDGE('',*,*,#13554,.T.);
#18012=ORIENTED_EDGE('',*,*,#13553,.F.);
#18013=ORIENTED_EDGE('',*,*,#13554,.F.);
#18014=ORIENTED_EDGE('',*,*,#13555,.F.);
#18015=ORIENTED_EDGE('',*,*,#13556,.F.);
#18016=ORIENTED_EDGE('',*,*,#13557,.F.);
#18017=ORIENTED_EDGE('',*,*,#13558,.F.);
#18018=ORIENTED_EDGE('',*,*,#13559,.F.);
#18019=ORIENTED_EDGE('',*,*,#13560,.F.);
#18020=ORIENTED_EDGE('',*,*,#13552,.F.);
#18021=ORIENTED_EDGE('',*,*,#13561,.F.);
#18022=ORIENTED_EDGE('',*,*,#13555,.T.);
#18023=ORIENTED_EDGE('',*,*,#13562,.T.);
#18024=ORIENTED_EDGE('',*,*,#13551,.F.);
#18025=ORIENTED_EDGE('',*,*,#13563,.F.);
#18026=ORIENTED_EDGE('',*,*,#13556,.T.);
#18027=ORIENTED_EDGE('',*,*,#13561,.T.);
#18028=ORIENTED_EDGE('',*,*,#13550,.F.);
#18029=ORIENTED_EDGE('',*,*,#13564,.F.);
#18030=ORIENTED_EDGE('',*,*,#13557,.T.);
#18031=ORIENTED_EDGE('',*,*,#13563,.T.);
#18032=ORIENTED_EDGE('',*,*,#13549,.F.);
#18033=ORIENTED_EDGE('',*,*,#13565,.F.);
#18034=ORIENTED_EDGE('',*,*,#13558,.T.);
#18035=ORIENTED_EDGE('',*,*,#13564,.T.);
#18036=ORIENTED_EDGE('',*,*,#13548,.F.);
#18037=ORIENTED_EDGE('',*,*,#13566,.F.);
#18038=ORIENTED_EDGE('',*,*,#13559,.T.);
#18039=ORIENTED_EDGE('',*,*,#13565,.T.);
#18040=ORIENTED_EDGE('',*,*,#13547,.F.);
#18041=ORIENTED_EDGE('',*,*,#13562,.F.);
#18042=ORIENTED_EDGE('',*,*,#13560,.T.);
#18043=ORIENTED_EDGE('',*,*,#13566,.T.);
#22845=CYLINDRICAL_SURFACE('',#25649,2.5);
#23614=ADVANCED_FACE('',(#2622,#1138),#1541,.T.);
#23615=ADVANCED_FACE('',(#2623),#1542,.T.);
#23616=ADVANCED_FACE('',(#2624),#22845,.T.);
#23617=ADVANCED_FACE('',(#2625),#1543,.F.);
#23618=ADVANCED_FACE('',(#2626),#1544,.F.);
#23619=ADVANCED_FACE('',(#2627),#1545,.F.);
#23620=ADVANCED_FACE('',(#2628),#1546,.F.);
#23621=ADVANCED_FACE('',(#2629),#1547,.F.);
#23622=ADVANCED_FACE('',(#2630),#1548,.F.);
#23623=ADVANCED_FACE('',(#2631),#1549,.F.);
#24540=CLOSED_SHELL('',(#23614,#23615,#23616,#23617,#23618,#23619,#23620,
#23621,#23622,#23623));
#25644=AXIS2_PLACEMENT_3D('',#51659,#29468,#29469);
#25645=AXIS2_PLACEMENT_3D('',#51660,#29470,#29471);
#25646=AXIS2_PLACEMENT_3D('',#51662,#29472,#29473);
#25647=AXIS2_PLACEMENT_3D('',#51675,#29480,#29481);
#25648=AXIS2_PLACEMENT_3D('',#51677,#29482,#29483);
#25649=AXIS2_PLACEMENT_3D('',#51678,#29484,#29485);
#25650=AXIS2_PLACEMENT_3D('',#51680,#29487,#29488);
#25651=AXIS2_PLACEMENT_3D('',#51693,#29495,#29496);
#25652=AXIS2_PLACEMENT_3D('',#51696,#29499,#29500);
#25653=AXIS2_PLACEMENT_3D('',#51698,#29502,#29503);
#25654=AXIS2_PLACEMENT_3D('',#51700,#29505,#29506);
#25655=AXIS2_PLACEMENT_3D('',#51702,#29508,#29509);
#25656=AXIS2_PLACEMENT_3D('',#51704,#29511,#29512);
#29468=DIRECTION('axis',(0.,0.,1.));
#29469=DIRECTION('refdir',(1.,0.,0.));
#29470=DIRECTION('center_axis',(0.,0.,1.));
#29471=DIRECTION('ref_axis',(1.,0.,0.));
#29472=DIRECTION('center_axis',(0.,0.,1.));
#29473=DIRECTION('ref_axis',(-1.,0.,0.));
#29474=DIRECTION('',(-0.866025403761798,0.500000000039214,0.));
#29475=DIRECTION('',(0.,1.,0.));
#29476=DIRECTION('',(0.866025403761798,0.500000000039214,0.));
#29477=DIRECTION('',(0.866025403761798,-0.500000000039214,0.));
#29478=DIRECTION('',(0.,-1.,0.));
#29479=DIRECTION('',(-0.866025403761798,-0.500000000039214,0.));
#29480=DIRECTION('center_axis',(0.,0.,-1.));
#29481=DIRECTION('ref_axis',(0.,-1.,0.));
#29482=DIRECTION('center_axis',(0.,0.,-1.));
#29483=DIRECTION('ref_axis',(-1.,0.,0.));
#29484=DIRECTION('center_axis',(0.,0.,1.));
#29485=DIRECTION('ref_axis',(-1.,0.,0.));
#29486=DIRECTION('',(0.,0.,-1.));
#29487=DIRECTION('center_axis',(0.,0.,-1.));
#29488=DIRECTION('ref_axis',(0.,-1.,0.));
#29489=DIRECTION('',(-0.866025403761798,-0.500000000039214,0.));
#29490=DIRECTION('',(0.,-1.,0.));
#29491=DIRECTION('',(0.866025403761798,-0.500000000039214,0.));
#29492=DIRECTION('',(0.866025403761798,0.500000000039214,0.));
#29493=DIRECTION('',(0.,1.,0.));
#29494=DIRECTION('',(-0.866025403761798,0.500000000039214,0.));
#29495=DIRECTION('center_axis',(0.500000000039214,-0.866025403761798,0.));
#29496=DIRECTION('ref_axis',(0.,0.,-1.));
#29497=DIRECTION('',(0.,0.,1.));
#29498=DIRECTION('',(0.,0.,1.));
#29499=DIRECTION('center_axis',(1.,0.,0.));
#29500=DIRECTION('ref_axis',(0.,1.,0.));
#29501=DIRECTION('',(0.,0.,1.));
#29502=DIRECTION('center_axis',(0.500000000039214,0.866025403761798,0.));
#29503=DIRECTION('ref_axis',(0.,0.,-1.));
#29504=DIRECTION('',(0.,0.,1.));
#29505=DIRECTION('center_axis',(-0.500000000039214,0.866025403761798,0.));
#29506=DIRECTION('ref_axis',(0.,0.,1.));
#29507=DIRECTION('',(0.,0.,1.));
#29508=DIRECTION('center_axis',(-1.,0.,0.));
#29509=DIRECTION('ref_axis',(0.,0.,1.));
#29510=DIRECTION('',(0.,0.,1.));
#29511=DIRECTION('center_axis',(-0.500000000039214,-0.866025403761798,0.));
#29512=DIRECTION('ref_axis',(-0.866025403761798,0.500000000039214,0.));
#51659=CARTESIAN_POINT('',(0.,0.,0.));
#51660=CARTESIAN_POINT('Origin',(23.,0.,19.3));
#51661=CARTESIAN_POINT('',(25.5,-3.06161699786838E-16,19.3));
#51662=CARTESIAN_POINT('Origin',(23.,0.,19.3));
#51663=CARTESIAN_POINT('',(23.,-1.3856406461,19.3));
#51664=CARTESIAN_POINT('',(21.8,-0.692820323,19.3));
#51665=CARTESIAN_POINT('',(22.3999999999746,-1.03923048453533,19.3));
#51666=CARTESIAN_POINT('',(21.8,0.692820323,19.3));
#51667=CARTESIAN_POINT('',(21.8,0.17320508075,19.3));
#51668=CARTESIAN_POINT('',(23.,1.3856406461,19.3));
#51669=CARTESIAN_POINT('',(22.3999999999746,1.03923048453533,19.3));
#51670=CARTESIAN_POINT('',(24.2,0.692820323,19.3));
#51671=CARTESIAN_POINT('',(23.6000000000254,1.03923048453533,19.3));
#51672=CARTESIAN_POINT('',(24.2,-0.692820323,19.3));
#51673=CARTESIAN_POINT('',(24.2,0.,19.3));
#51674=CARTESIAN_POINT('',(23.6000000000254,-1.03923048453533,19.3));
#51675=CARTESIAN_POINT('Origin',(23.,0.,9.3));
#51676=CARTESIAN_POINT('',(25.5,-3.06161699786838E-16,9.3));
#51677=CARTESIAN_POINT('Origin',(23.,0.,9.3));
#51678=CARTESIAN_POINT('Origin',(23.,0.,14.3));
#51679=CARTESIAN_POINT('',(25.5,3.06161699786838E-16,14.3));
#51680=CARTESIAN_POINT('Origin',(23.,3.11198878113149E-17,16.8));
#51681=CARTESIAN_POINT('',(24.2,-0.692820323,16.8));
#51682=CARTESIAN_POINT('',(23.,-1.3856406461,16.8));
#51683=CARTESIAN_POINT('',(24.2,-0.692820323,16.8));
#51684=CARTESIAN_POINT('',(24.2,0.692820323,16.8));
#51685=CARTESIAN_POINT('',(24.2,0.692820323,16.8));
#51686=CARTESIAN_POINT('',(23.,1.3856406461,16.8));
#51687=CARTESIAN_POINT('',(23.,1.3856406461,16.8));
#51688=CARTESIAN_POINT('',(21.8,0.692820323,16.8));
#51689=CARTESIAN_POINT('',(21.8,0.692820323,16.8));
#51690=CARTESIAN_POINT('',(21.8,-0.692820323,16.8));
#51691=CARTESIAN_POINT('',(21.8,-0.692820323,16.8));
#51692=CARTESIAN_POINT('',(23.,-1.3856406461,16.8));
#51693=CARTESIAN_POINT('Origin',(23.6,-1.03923048455,16.8));
#51694=CARTESIAN_POINT('',(24.2,-0.692820323,16.8));
#51695=CARTESIAN_POINT('',(23.,-1.3856406461,16.8));
#51696=CARTESIAN_POINT('Origin',(24.2,0.,16.8));
#51697=CARTESIAN_POINT('',(24.2,0.692820323,16.8));
#51698=CARTESIAN_POINT('Origin',(23.6,1.03923048455,16.8));
#51699=CARTESIAN_POINT('',(23.,1.3856406461,16.8));
#51700=CARTESIAN_POINT('Origin',(22.4,1.03923048455,16.8));
#51701=CARTESIAN_POINT('',(21.8,0.692820323,16.8));
#51702=CARTESIAN_POINT('Origin',(21.8,0.3464101615,16.8));
#51703=CARTESIAN_POINT('',(21.8,-0.692820323,16.8));
#51704=CARTESIAN_POINT('Origin',(22.4,-1.03923048455,16.8));
#57021=UNCERTAINTY_MEASURE_WITH_UNIT(LENGTH_MEASURE(0.01),#57080,
'DISTANCE_ACCURACY_VALUE',
'Maximum model space distance between geometric entities at asserted c
onnectivities');
#57040=UNCERTAINTY_MEASURE_WITH_UNIT(LENGTH_MEASURE(0.01),#57080,
'DISTANCE_ACCURACY_VALUE',
'Maximum model space distance between geometric entities at asserted c
onnectivities');
#57060=(
GEOMETRIC_REPRESENTATION_CONTEXT(3)
GLOBAL_UNCERTAINTY_ASSIGNED_CONTEXT((#57021))
GLOBAL_UNIT_ASSIGNED_CONTEXT((#57080,#57082,#57083))
REPRESENTATION_CONTEXT('','3D')
);
#57079=(
GEOMETRIC_REPRESENTATION_CONTEXT(3)
GLOBAL_UNCERTAINTY_ASSIGNED_CONTEXT((#57040))
GLOBAL_UNIT_ASSIGNED_CONTEXT((#57080,#57082,#57083))
REPRESENTATION_CONTEXT('','3D')
);
#57080=(
LENGTH_UNIT()
NAMED_UNIT(*)
SI_UNIT(.MILLI.,.METRE.)
);
#57082=(
NAMED_UNIT(*)
PLANE_ANGLE_UNIT()
SI_UNIT($,.RADIAN.)
);
#57083=(
NAMED_UNIT(*)
SI_UNIT($,.STERADIAN.)
SOLID_ANGLE_UNIT()
);
#57103=SHAPE_DEFINITION_REPRESENTATION(#57149,#57268);
#57149=PRODUCT_DEFINITION_SHAPE('',$,#57307);
#57268=SHAPE_REPRESENTATION('',(#25644),#57060);
#57287=PRODUCT_DEFINITION_CONTEXT('part definition',#57403,'design');
#57307=PRODUCT_DEFINITION('Coupling Set Screw 1','Coupling Set Screw 1',
#57345,#57287);
#57345=PRODUCT_DEFINITION_FORMATION('',$,#57424);
#57403=APPLICATION_CONTEXT(
'Core Data for Automotive Mechanical Design Process');
#57404=PRODUCT_CONTEXT('part definition',#57403,'mechanical');
#57424=PRODUCT('Coupling Set Screw 1','Coupling Set Screw 1',$,(#57404));
#57444=PRESENTATION_STYLE_ASSIGNMENT((#57446));
#57446=SURFACE_STYLE_USAGE(.BOTH.,#57448);
#57448=SURFACE_SIDE_STYLE('',(#57450));
#57450=SURFACE_STYLE_FILL_AREA(#57452);
#57452=FILL_AREA_STYLE('Opaque(202,209,238)',(#57454));
#57454=FILL_AREA_STYLE_COLOUR('Opaque(202,209,238)',#57456);
#57456=COLOUR_RGB('Opaque(202,209,238)',0.792156862745098,0.819607843137255,
0.933333333333333);
ENDSEC;
END-ISO-10303-21;
